ISO-10303-21;
HEADER;
/* Generated by software containing ST-Developer
 * from STEP Tools, Inc. (www.steptools.com) 
 */

FILE_DESCRIPTION(
/* description */ ('Bin tilter linkage'),
/* implementation_level */ '2;1');

FILE_NAME(
/* name */ 'Screw and guide support.step',
/* time_stamp */ '2026-10-28T03:26:24-07:00',
/* author */ (''),
/* organization */ (''),
/* preprocessor_version */ 'ST-DEVELOPER v20.2',
/* originating_system */ 'Autodesk Translation Framework v15.17.0.0',
/* authorisation */ '');

FILE_SCHEMA (('AUTOMOTIVE_DESIGN { 1 0 10303 214 3 1 1 }'));
ENDSEC;

DATA;
#10=MECHANICAL_DESIGN_GEOMETRIC_PRESENTATION_REPRESENTATION('',(#875),#23728);
#663=SHAPE_REPRESENTATION_RELATIONSHIP('SRR','None',#24127,#769);
#769=ADVANCED_BREP_SHAPE_REPRESENTATION('',(#989),#23627);
#875=STYLED_ITEM('',(#24772),#989);
#989=MANIFOLD_SOLID_BREP('Body1',#12405);
#1173=FACE_BOUND('',#2870,.T.);
#1174=FACE_BOUND('',#2872,.T.);
#1175=FACE_BOUND('',#2873,.T.);
#1176=FACE_BOUND('',#2874,.T.);
#1177=FACE_BOUND('',#2875,.T.);
#1178=FACE_BOUND('',#2878,.T.);
#1179=FACE_BOUND('',#2882,.T.);
#1180=FACE_BOUND('',#2890,.T.);
#1181=FACE_BOUND('',#2891,.T.);
#1182=FACE_BOUND('',#2892,.T.);
#1183=FACE_BOUND('',#2893,.T.);
#1184=FACE_BOUND('',#2895,.T.);
#1185=FACE_BOUND('',#2897,.T.);
#1186=FACE_BOUND('',#2898,.T.);
#1552=PLANE('',#13920);
#1553=PLANE('',#13922);
#1554=PLANE('',#13929);
#1555=PLANE('',#13935);
#1556=PLANE('',#13945);
#1557=PLANE('',#13946);
#1558=PLANE('',#13947);
#1559=PLANE('',#13948);
#1560=PLANE('',#13949);
#2004=FACE_OUTER_BOUND('',#2867,.T.);
#2005=FACE_OUTER_BOUND('',#2868,.T.);
#2006=FACE_OUTER_BOUND('',#2869,.T.);
#2007=FACE_OUTER_BOUND('',#2871,.T.);
#2008=FACE_OUTER_BOUND('',#2876,.T.);
#2009=FACE_OUTER_BOUND('',#2877,.T.);
#2010=FACE_OUTER_BOUND('',#2879,.T.);
#2011=FACE_OUTER_BOUND('',#2880,.T.);
#2012=FACE_OUTER_BOUND('',#2881,.T.);
#2013=FACE_OUTER_BOUND('',#2883,.T.);
#2014=FACE_OUTER_BOUND('',#2884,.T.);
#2015=FACE_OUTER_BOUND('',#2885,.T.);
#2016=FACE_OUTER_BOUND('',#2886,.T.);
#2017=FACE_OUTER_BOUND('',#2887,.T.);
#2018=FACE_OUTER_BOUND('',#2888,.T.);
#2019=FACE_OUTER_BOUND('',#2889,.T.);
#2020=FACE_OUTER_BOUND('',#2894,.T.);
#2021=FACE_OUTER_BOUND('',#2896,.T.);
#2867=EDGE_LOOP('',(#8865,#8866,#8867,#8868));
#2868=EDGE_LOOP('',(#8869,#8870,#8871,#8872));
#2869=EDGE_LOOP('',(#8873,#8874,#8875,#8876));
#2870=EDGE_LOOP('',(#8877));
#2871=EDGE_LOOP('',(#8878,#8879,#8880,#8881,#8882,#8883));
#2872=EDGE_LOOP('',(#8884));
#2873=EDGE_LOOP('',(#8885));
#2874=EDGE_LOOP('',(#8886));
#2875=EDGE_LOOP('',(#8887));
#2876=EDGE_LOOP('',(#8888,#8889,#8890,#8891));
#2877=EDGE_LOOP('',(#8892));
#2878=EDGE_LOOP('',(#8893));
#2879=EDGE_LOOP('',(#8894,#8895,#8896,#8897));
#2880=EDGE_LOOP('',(#8898,#8899,#8900,#8901));
#2881=EDGE_LOOP('',(#8902));
#2882=EDGE_LOOP('',(#8903));
#2883=EDGE_LOOP('',(#8904,#8905,#8906,#8907));
#2884=EDGE_LOOP('',(#8908,#8909,#8910,#8911));
#2885=EDGE_LOOP('',(#8912,#8913,#8914,#8915));
#2886=EDGE_LOOP('',(#8916,#8917,#8918,#8919));
#2887=EDGE_LOOP('',(#8920,#8921,#8922,#8923));
#2888=EDGE_LOOP('',(#8924,#8925,#8926,#8927));
#2889=EDGE_LOOP('',(#8928,#8929,#8930,#8931,#8932,#8933));
#2890=EDGE_LOOP('',(#8934));
#2891=EDGE_LOOP('',(#8935));
#2892=EDGE_LOOP('',(#8936));
#2893=EDGE_LOOP('',(#8937));
#2894=EDGE_LOOP('',(#8938,#8939,#8940,#8941));
#2895=EDGE_LOOP('',(#8942));
#2896=EDGE_LOOP('',(#8943,#8944,#8945,#8946));
#2897=EDGE_LOOP('',(#8947));
#2898=EDGE_LOOP('',(#8948));
#3987=LINE('',#20290,#4662);
#3988=LINE('',#20293,#4663);
#3989=LINE('',#20298,#4664);
#3990=LINE('',#20302,#4665);
#3991=LINE('',#20304,#4666);
#3992=LINE('',#20305,#4667);
#3993=LINE('',#20310,#4668);
#3994=LINE('',#20312,#4669);
#3995=LINE('',#20314,#4670);
#3996=LINE('',#20315,#4671);
#3997=LINE('',#20326,#4672);
#3998=LINE('',#20334,#4673);
#3999=LINE('',#20338,#4674);
#4000=LINE('',#20345,#4675);
#4001=LINE('',#20349,#4676);
#4002=LINE('',#20353,#4677);
#4003=LINE('',#20357,#4678);
#4004=LINE('',#20360,#4679);
#4005=LINE('',#20362,#4680);
#4006=LINE('',#20363,#4681);
#4007=LINE('',#20366,#4682);
#4008=LINE('',#20367,#4683);
#4009=LINE('',#20369,#4684);
#4010=LINE('',#20370,#4685);
#4662=VECTOR('',#16092,1.);
#4663=VECTOR('',#16095,1.);
#4664=VECTOR('',#16100,0.165);
#4665=VECTOR('',#16105,1.);
#4666=VECTOR('',#16106,1.);
#4667=VECTOR('',#16107,1.);
#4668=VECTOR('',#16112,1.);
#4669=VECTOR('',#16113,1.);
#4670=VECTOR('',#16114,1.);
#4671=VECTOR('',#16115,1.);
#4672=VECTOR('',#16126,0.4);
#4673=VECTOR('',#16137,0.225);
#4674=VECTOR('',#16142,0.4);
#4675=VECTOR('',#16151,0.225);
#4676=VECTOR('',#16156,1.6);
#4677=VECTOR('',#16161,0.605);
#4678=VECTOR('',#16166,0.605);
#4679=VECTOR('',#16169,1.);
#4680=VECTOR('',#16170,1.);
#4681=VECTOR('',#16171,1.);
#4682=VECTOR('',#16174,1.);
#4683=VECTOR('',#16175,1.);
#4684=VECTOR('',#16178,1.);
#4685=VECTOR('',#16179,1.);
#5307=CIRCLE('',#13915,0.164999999999999);
#5308=CIRCLE('',#13916,0.164999999999999);
#5309=CIRCLE('',#13918,0.165);
#5310=CIRCLE('',#13919,0.165);
#5311=CIRCLE('',#13921,0.4);
#5312=CIRCLE('',#13923,0.605);
#5313=CIRCLE('',#13924,0.605);
#5314=CIRCLE('',#13925,1.6);
#5315=CIRCLE('',#13927,0.4);
#5316=CIRCLE('',#13928,0.4);
#5317=CIRCLE('',#13930,0.225);
#5318=CIRCLE('',#13932,0.225);
#5319=CIRCLE('',#13934,0.4);
#5320=CIRCLE('',#13936,0.225);
#5321=CIRCLE('',#13938,0.225);
#5322=CIRCLE('',#13940,1.6);
#5323=CIRCLE('',#13942,0.605);
#5324=CIRCLE('',#13944,0.605);
#6121=VERTEX_POINT('',#20286);
#6122=VERTEX_POINT('',#20287);
#6123=VERTEX_POINT('',#20289);
#6124=VERTEX_POINT('',#20291);
#6125=VERTEX_POINT('',#20295);
#6126=VERTEX_POINT('',#20297);
#6127=VERTEX_POINT('',#20301);
#6128=VERTEX_POINT('',#20303);
#6129=VERTEX_POINT('',#20306);
#6130=VERTEX_POINT('',#20309);
#6131=VERTEX_POINT('',#20311);
#6132=VERTEX_POINT('',#20313);
#6133=VERTEX_POINT('',#20316);
#6134=VERTEX_POINT('',#20318);
#6135=VERTEX_POINT('',#20320);
#6136=VERTEX_POINT('',#20323);
#6137=VERTEX_POINT('',#20325);
#6138=VERTEX_POINT('',#20329);
#6139=VERTEX_POINT('',#20332);
#6140=VERTEX_POINT('',#20336);
#6141=VERTEX_POINT('',#20340);
#6142=VERTEX_POINT('',#20343);
#6143=VERTEX_POINT('',#20347);
#6144=VERTEX_POINT('',#20351);
#6145=VERTEX_POINT('',#20355);
#6146=VERTEX_POINT('',#20359);
#6147=VERTEX_POINT('',#20361);
#6148=VERTEX_POINT('',#20365);
#7172=EDGE_CURVE('',#6121,#6122,#5307,.T.);
#7173=EDGE_CURVE('',#6123,#6121,#3987,.T.);
#7174=EDGE_CURVE('',#6124,#6123,#5308,.T.);
#7175=EDGE_CURVE('',#6122,#6124,#3988,.T.);
#7176=EDGE_CURVE('',#6125,#6125,#5309,.T.);
#7177=EDGE_CURVE('',#6125,#6126,#3989,.T.);
#7178=EDGE_CURVE('',#6126,#6126,#5310,.T.);
#7179=EDGE_CURVE('',#6121,#6127,#3990,.T.);
#7180=EDGE_CURVE('',#6127,#6128,#3991,.T.);
#7181=EDGE_CURVE('',#6128,#6123,#3992,.T.);
#7182=EDGE_CURVE('',#6129,#6129,#5311,.T.);
#7183=EDGE_CURVE('',#6130,#6128,#3993,.T.);
#7184=EDGE_CURVE('',#6130,#6131,#3994,.T.);
#7185=EDGE_CURVE('',#6131,#6132,#3995,.T.);
#7186=EDGE_CURVE('',#6124,#6132,#3996,.T.);
#7187=EDGE_CURVE('',#6133,#6133,#5312,.T.);
#7188=EDGE_CURVE('',#6134,#6134,#5313,.T.);
#7189=EDGE_CURVE('',#6135,#6135,#5314,.T.);
#7190=EDGE_CURVE('',#6136,#6136,#5315,.T.);
#7191=EDGE_CURVE('',#6136,#6137,#3997,.T.);
#7192=EDGE_CURVE('',#6137,#6137,#5316,.T.);
#7193=EDGE_CURVE('',#6138,#6138,#5317,.T.);
#7194=EDGE_CURVE('',#6139,#6139,#5318,.T.);
#7195=EDGE_CURVE('',#6139,#6138,#3998,.T.);
#7196=EDGE_CURVE('',#6140,#6140,#5319,.T.);
#7197=EDGE_CURVE('',#6140,#6129,#3999,.T.);
#7198=EDGE_CURVE('',#6141,#6141,#5320,.T.);
#7199=EDGE_CURVE('',#6142,#6142,#5321,.T.);
#7200=EDGE_CURVE('',#6142,#6141,#4000,.T.);
#7201=EDGE_CURVE('',#6143,#6143,#5322,.T.);
#7202=EDGE_CURVE('',#6143,#6135,#4001,.T.);
#7203=EDGE_CURVE('',#6144,#6144,#5323,.T.);
#7204=EDGE_CURVE('',#6144,#6134,#4002,.T.);
#7205=EDGE_CURVE('',#6145,#6145,#5324,.T.);
#7206=EDGE_CURVE('',#6145,#6133,#4003,.T.);
#7207=EDGE_CURVE('',#6131,#6146,#4004,.T.);
#7208=EDGE_CURVE('',#6146,#6147,#4005,.T.);
#7209=EDGE_CURVE('',#6132,#6147,#4006,.T.);
#7210=EDGE_CURVE('',#6148,#6130,#4007,.T.);
#7211=EDGE_CURVE('',#6148,#6127,#4008,.T.);
#7212=EDGE_CURVE('',#6147,#6122,#4009,.T.);
#7213=EDGE_CURVE('',#6146,#6148,#4010,.T.);
#8865=ORIENTED_EDGE('',*,*,#7172,.F.);
#8866=ORIENTED_EDGE('',*,*,#7173,.F.);
#8867=ORIENTED_EDGE('',*,*,#7174,.F.);
#8868=ORIENTED_EDGE('',*,*,#7175,.F.);
#8869=ORIENTED_EDGE('',*,*,#7176,.F.);
#8870=ORIENTED_EDGE('',*,*,#7177,.T.);
#8871=ORIENTED_EDGE('',*,*,#7178,.F.);
#8872=ORIENTED_EDGE('',*,*,#7177,.F.);
#8873=ORIENTED_EDGE('',*,*,#7173,.T.);
#8874=ORIENTED_EDGE('',*,*,#7179,.T.);
#8875=ORIENTED_EDGE('',*,*,#7180,.T.);
#8876=ORIENTED_EDGE('',*,*,#7181,.T.);
#8877=ORIENTED_EDGE('',*,*,#7182,.T.);
#8878=ORIENTED_EDGE('',*,*,#7174,.T.);
#8879=ORIENTED_EDGE('',*,*,#7181,.F.);
#8880=ORIENTED_EDGE('',*,*,#7183,.F.);
#8881=ORIENTED_EDGE('',*,*,#7184,.T.);
#8882=ORIENTED_EDGE('',*,*,#7185,.T.);
#8883=ORIENTED_EDGE('',*,*,#7186,.F.);
#8884=ORIENTED_EDGE('',*,*,#7187,.T.);
#8885=ORIENTED_EDGE('',*,*,#7188,.T.);
#8886=ORIENTED_EDGE('',*,*,#7189,.T.);
#8887=ORIENTED_EDGE('',*,*,#7178,.T.);
#8888=ORIENTED_EDGE('',*,*,#7190,.F.);
#8889=ORIENTED_EDGE('',*,*,#7191,.T.);
#8890=ORIENTED_EDGE('',*,*,#7192,.F.);
#8891=ORIENTED_EDGE('',*,*,#7191,.F.);
#8892=ORIENTED_EDGE('',*,*,#7190,.T.);
#8893=ORIENTED_EDGE('',*,*,#7193,.F.);
#8894=ORIENTED_EDGE('',*,*,#7194,.F.);
#8895=ORIENTED_EDGE('',*,*,#7195,.T.);
#8896=ORIENTED_EDGE('',*,*,#7193,.T.);
#8897=ORIENTED_EDGE('',*,*,#7195,.F.);
#8898=ORIENTED_EDGE('',*,*,#7196,.F.);
#8899=ORIENTED_EDGE('',*,*,#7197,.T.);
#8900=ORIENTED_EDGE('',*,*,#7182,.F.);
#8901=ORIENTED_EDGE('',*,*,#7197,.F.);
#8902=ORIENTED_EDGE('',*,*,#7196,.T.);
#8903=ORIENTED_EDGE('',*,*,#7198,.F.);
#8904=ORIENTED_EDGE('',*,*,#7199,.F.);
#8905=ORIENTED_EDGE('',*,*,#7200,.T.);
#8906=ORIENTED_EDGE('',*,*,#7198,.T.);
#8907=ORIENTED_EDGE('',*,*,#7200,.F.);
#8908=ORIENTED_EDGE('',*,*,#7201,.F.);
#8909=ORIENTED_EDGE('',*,*,#7202,.T.);
#8910=ORIENTED_EDGE('',*,*,#7189,.F.);
#8911=ORIENTED_EDGE('',*,*,#7202,.F.);
#8912=ORIENTED_EDGE('',*,*,#7203,.F.);
#8913=ORIENTED_EDGE('',*,*,#7204,.T.);
#8914=ORIENTED_EDGE('',*,*,#7188,.F.);
#8915=ORIENTED_EDGE('',*,*,#7204,.F.);
#8916=ORIENTED_EDGE('',*,*,#7205,.F.);
#8917=ORIENTED_EDGE('',*,*,#7206,.T.);
#8918=ORIENTED_EDGE('',*,*,#7187,.F.);
#8919=ORIENTED_EDGE('',*,*,#7206,.F.);
#8920=ORIENTED_EDGE('',*,*,#7207,.T.);
#8921=ORIENTED_EDGE('',*,*,#7208,.T.);
#8922=ORIENTED_EDGE('',*,*,#7209,.F.);
#8923=ORIENTED_EDGE('',*,*,#7185,.F.);
#8924=ORIENTED_EDGE('',*,*,#7210,.T.);
#8925=ORIENTED_EDGE('',*,*,#7183,.T.);
#8926=ORIENTED_EDGE('',*,*,#7180,.F.);
#8927=ORIENTED_EDGE('',*,*,#7211,.F.);
#8928=ORIENTED_EDGE('',*,*,#7172,.T.);
#8929=ORIENTED_EDGE('',*,*,#7212,.F.);
#8930=ORIENTED_EDGE('',*,*,#7208,.F.);
#8931=ORIENTED_EDGE('',*,*,#7213,.T.);
#8932=ORIENTED_EDGE('',*,*,#7211,.T.);
#8933=ORIENTED_EDGE('',*,*,#7179,.F.);
#8934=ORIENTED_EDGE('',*,*,#7176,.T.);
#8935=ORIENTED_EDGE('',*,*,#7201,.T.);
#8936=ORIENTED_EDGE('',*,*,#7203,.T.);
#8937=ORIENTED_EDGE('',*,*,#7205,.T.);
#8938=ORIENTED_EDGE('',*,*,#7175,.T.);
#8939=ORIENTED_EDGE('',*,*,#7186,.T.);
#8940=ORIENTED_EDGE('',*,*,#7209,.T.);
#8941=ORIENTED_EDGE('',*,*,#7212,.T.);
#8942=ORIENTED_EDGE('',*,*,#7192,.T.);
#8943=ORIENTED_EDGE('',*,*,#7213,.F.);
#8944=ORIENTED_EDGE('',*,*,#7207,.F.);
#8945=ORIENTED_EDGE('',*,*,#7184,.F.);
#8946=ORIENTED_EDGE('',*,*,#7210,.F.);
#8947=ORIENTED_EDGE('',*,*,#7194,.T.);
#8948=ORIENTED_EDGE('',*,*,#7199,.T.);
#11321=CYLINDRICAL_SURFACE('',#13914,0.164999999999999);
#11322=CYLINDRICAL_SURFACE('',#13917,0.165);
#11323=CYLINDRICAL_SURFACE('',#13926,0.4);
#11324=CYLINDRICAL_SURFACE('',#13931,0.225);
#11325=CYLINDRICAL_SURFACE('',#13933,0.4);
#11326=CYLINDRICAL_SURFACE('',#13937,0.225);
#11327=CYLINDRICAL_SURFACE('',#13939,1.6);
#11328=CYLINDRICAL_SURFACE('',#13941,0.605);
#11329=CYLINDRICAL_SURFACE('',#13943,0.605);
#11729=ADVANCED_FACE('',(#2004),#11321,.F.);
#11730=ADVANCED_FACE('',(#2005),#11322,.F.);
#11731=ADVANCED_FACE('',(#2006,#1173),#1552,.T.);
#11732=ADVANCED_FACE('',(#2007,#1174,#1175,#1176,#1177),#1553,.T.);
#11733=ADVANCED_FACE('',(#2008),#11323,.F.);
#11734=ADVANCED_FACE('',(#2009,#1178),#1554,.T.);
#11735=ADVANCED_FACE('',(#2010),#11324,.F.);
#11736=ADVANCED_FACE('',(#2011),#11325,.F.);
#11737=ADVANCED_FACE('',(#2012,#1179),#1555,.T.);
#11738=ADVANCED_FACE('',(#2013),#11326,.F.);
#11739=ADVANCED_FACE('',(#2014),#11327,.F.);
#11740=ADVANCED_FACE('',(#2015),#11328,.F.);
#11741=ADVANCED_FACE('',(#2016),#11329,.F.);
#11742=ADVANCED_FACE('',(#2017),#1556,.T.);
#11743=ADVANCED_FACE('',(#2018),#1557,.T.);
#11744=ADVANCED_FACE('',(#2019,#1180,#1181,#1182,#1183),#1558,.T.);
#11745=ADVANCED_FACE('',(#2020,#1184),#1559,.T.);
#11746=ADVANCED_FACE('',(#2021,#1185,#1186),#1560,.F.);
#12405=CLOSED_SHELL('',(#11729,#11730,#11731,#11732,#11733,#11734,#11735,
#11736,#11737,#11738,#11739,#11740,#11741,#11742,#11743,#11744,#11745,#11746));
#13913=AXIS2_PLACEMENT_3D('',#20284,#16086,#16087);
#13914=AXIS2_PLACEMENT_3D('',#20285,#16088,#16089);
#13915=AXIS2_PLACEMENT_3D('',#20288,#16090,#16091);
#13916=AXIS2_PLACEMENT_3D('',#20292,#16093,#16094);
#13917=AXIS2_PLACEMENT_3D('',#20294,#16096,#16097);
#13918=AXIS2_PLACEMENT_3D('',#20296,#16098,#16099);
#13919=AXIS2_PLACEMENT_3D('',#20299,#16101,#16102);
#13920=AXIS2_PLACEMENT_3D('',#20300,#16103,#16104);
#13921=AXIS2_PLACEMENT_3D('',#20307,#16108,#16109);
#13922=AXIS2_PLACEMENT_3D('',#20308,#16110,#16111);
#13923=AXIS2_PLACEMENT_3D('',#20317,#16116,#16117);
#13924=AXIS2_PLACEMENT_3D('',#20319,#16118,#16119);
#13925=AXIS2_PLACEMENT_3D('',#20321,#16120,#16121);
#13926=AXIS2_PLACEMENT_3D('',#20322,#16122,#16123);
#13927=AXIS2_PLACEMENT_3D('',#20324,#16124,#16125);
#13928=AXIS2_PLACEMENT_3D('',#20327,#16127,#16128);
#13929=AXIS2_PLACEMENT_3D('',#20328,#16129,#16130);
#13930=AXIS2_PLACEMENT_3D('',#20330,#16131,#16132);
#13931=AXIS2_PLACEMENT_3D('',#20331,#16133,#16134);
#13932=AXIS2_PLACEMENT_3D('',#20333,#16135,#16136);
#13933=AXIS2_PLACEMENT_3D('',#20335,#16138,#16139);
#13934=AXIS2_PLACEMENT_3D('',#20337,#16140,#16141);
#13935=AXIS2_PLACEMENT_3D('',#20339,#16143,#16144);
#13936=AXIS2_PLACEMENT_3D('',#20341,#16145,#16146);
#13937=AXIS2_PLACEMENT_3D('',#20342,#16147,#16148);
#13938=AXIS2_PLACEMENT_3D('',#20344,#16149,#16150);
#13939=AXIS2_PLACEMENT_3D('',#20346,#16152,#16153);
#13940=AXIS2_PLACEMENT_3D('',#20348,#16154,#16155);
#13941=AXIS2_PLACEMENT_3D('',#20350,#16157,#16158);
#13942=AXIS2_PLACEMENT_3D('',#20352,#16159,#16160);
#13943=AXIS2_PLACEMENT_3D('',#20354,#16162,#16163);
#13944=AXIS2_PLACEMENT_3D('',#20356,#16164,#16165);
#13945=AXIS2_PLACEMENT_3D('',#20358,#16167,#16168);
#13946=AXIS2_PLACEMENT_3D('',#20364,#16172,#16173);
#13947=AXIS2_PLACEMENT_3D('',#20368,#16176,#16177);
#13948=AXIS2_PLACEMENT_3D('',#20371,#16180,#16181);
#13949=AXIS2_PLACEMENT_3D('',#20372,#16182,#16183);
#16086=DIRECTION('axis',(0.,0.,1.));
#16087=DIRECTION('refdir',(1.,0.,0.));
#16088=DIRECTION('center_axis',(1.,0.,0.));
#16089=DIRECTION('ref_axis',(0.,0.,-1.));
#16090=DIRECTION('center_axis',(1.,0.,0.));
#16091=DIRECTION('ref_axis',(0.,0.,-1.));
#16092=DIRECTION('',(-1.,0.,0.));
#16093=DIRECTION('center_axis',(-1.,0.,0.));
#16094=DIRECTION('ref_axis',(0.,0.,-1.));
#16095=DIRECTION('',(1.,0.,0.));
#16096=DIRECTION('center_axis',(1.,0.,0.));
#16097=DIRECTION('ref_axis',(0.,0.,-1.));
#16098=DIRECTION('center_axis',(1.,0.,0.));
#16099=DIRECTION('ref_axis',(0.,0.,-1.));
#16100=DIRECTION('',(1.,0.,0.));
#16101=DIRECTION('center_axis',(-1.,0.,0.));
#16102=DIRECTION('ref_axis',(0.,0.,-1.));
#16103=DIRECTION('center_axis',(0.,0.,1.));
#16104=DIRECTION('ref_axis',(1.,0.,0.));
#16105=DIRECTION('',(0.,-1.,0.));
#16106=DIRECTION('',(1.,0.,0.));
#16107=DIRECTION('',(0.,1.,0.));
#16108=DIRECTION('center_axis',(0.,0.,-1.));
#16109=DIRECTION('ref_axis',(1.,0.,0.));
#16110=DIRECTION('center_axis',(1.,0.,0.));
#16111=DIRECTION('ref_axis',(0.,1.,0.));
#16112=DIRECTION('',(0.,0.,1.));
#16113=DIRECTION('',(0.,1.,0.));
#16114=DIRECTION('',(0.,0.,1.));
#16115=DIRECTION('',(0.,1.,0.));
#16116=DIRECTION('center_axis',(-1.,0.,0.));
#16117=DIRECTION('ref_axis',(0.,0.,-1.));
#16118=DIRECTION('center_axis',(-1.,0.,0.));
#16119=DIRECTION('ref_axis',(0.,0.,-1.));
#16120=DIRECTION('center_axis',(-1.,0.,0.));
#16121=DIRECTION('ref_axis',(0.,0.,-1.));
#16122=DIRECTION('center_axis',(0.,0.,1.));
#16123=DIRECTION('ref_axis',(1.,0.,0.));
#16124=DIRECTION('center_axis',(0.,0.,1.));
#16125=DIRECTION('ref_axis',(1.,0.,0.));
#16126=DIRECTION('',(0.,0.,1.));
#16127=DIRECTION('center_axis',(0.,0.,-1.));
#16128=DIRECTION('ref_axis',(1.,0.,0.));
#16129=DIRECTION('center_axis',(0.,0.,1.));
#16130=DIRECTION('ref_axis',(1.,0.,0.));
#16131=DIRECTION('center_axis',(0.,0.,1.));
#16132=DIRECTION('ref_axis',(1.,0.,0.));
#16133=DIRECTION('center_axis',(0.,0.,1.));
#16134=DIRECTION('ref_axis',(1.,0.,0.));
#16135=DIRECTION('center_axis',(0.,0.,1.));
#16136=DIRECTION('ref_axis',(1.,0.,0.));
#16137=DIRECTION('',(0.,0.,1.));
#16138=DIRECTION('center_axis',(0.,0.,1.));
#16139=DIRECTION('ref_axis',(1.,0.,0.));
#16140=DIRECTION('center_axis',(0.,0.,1.));
#16141=DIRECTION('ref_axis',(1.,0.,0.));
#16142=DIRECTION('',(0.,0.,1.));
#16143=DIRECTION('center_axis',(0.,0.,1.));
#16144=DIRECTION('ref_axis',(1.,0.,0.));
#16145=DIRECTION('center_axis',(0.,0.,1.));
#16146=DIRECTION('ref_axis',(1.,0.,0.));
#16147=DIRECTION('center_axis',(0.,0.,1.));
#16148=DIRECTION('ref_axis',(1.,0.,0.));
#16149=DIRECTION('center_axis',(0.,0.,1.));
#16150=DIRECTION('ref_axis',(1.,0.,0.));
#16151=DIRECTION('',(0.,0.,1.));
#16152=DIRECTION('center_axis',(1.,0.,0.));
#16153=DIRECTION('ref_axis',(0.,0.,-1.));
#16154=DIRECTION('center_axis',(1.,0.,0.));
#16155=DIRECTION('ref_axis',(0.,0.,-1.));
#16156=DIRECTION('',(1.,0.,0.));
#16157=DIRECTION('center_axis',(1.,0.,0.));
#16158=DIRECTION('ref_axis',(0.,0.,-1.));
#16159=DIRECTION('center_axis',(1.,0.,0.));
#16160=DIRECTION('ref_axis',(0.,0.,-1.));
#16161=DIRECTION('',(1.,0.,0.));
#16162=DIRECTION('center_axis',(1.,0.,0.));
#16163=DIRECTION('ref_axis',(0.,0.,-1.));
#16164=DIRECTION('center_axis',(1.,0.,0.));
#16165=DIRECTION('ref_axis',(0.,0.,-1.));
#16166=DIRECTION('',(1.,0.,0.));
#16167=DIRECTION('center_axis',(0.,1.,0.));
#16168=DIRECTION('ref_axis',(-1.,0.,0.));
#16169=DIRECTION('',(-1.,0.,0.));
#16170=DIRECTION('',(0.,0.,1.));
#16171=DIRECTION('',(-1.,0.,0.));
#16172=DIRECTION('center_axis',(0.,-1.,0.));
#16173=DIRECTION('ref_axis',(1.,0.,0.));
#16174=DIRECTION('',(1.,0.,0.));
#16175=DIRECTION('',(0.,0.,1.));
#16176=DIRECTION('center_axis',(-1.,0.,0.));
#16177=DIRECTION('ref_axis',(0.,-1.,0.));
#16178=DIRECTION('',(0.,-1.,0.));
#16179=DIRECTION('',(0.,-1.,0.));
#16180=DIRECTION('center_axis',(0.,0.,1.));
#16181=DIRECTION('ref_axis',(1.,0.,0.));
#16182=DIRECTION('center_axis',(0.,0.,1.));
#16183=DIRECTION('ref_axis',(1.,0.,0.));
#20284=CARTESIAN_POINT('',(0.,0.,0.));
#20285=CARTESIAN_POINT('Origin',(-10.1,-4.5,9.85));
#20286=CARTESIAN_POINT('',(-10.,-4.56873863542434,10.));
#20287=CARTESIAN_POINT('',(-10.,-4.43126136457566,10.));
#20288=CARTESIAN_POINT('Origin',(-10.,-4.5,9.85));
#20289=CARTESIAN_POINT('',(-9.,-4.56873863542434,10.));
#20290=CARTESIAN_POINT('',(-10.1,-4.56873863542434,10.));
#20291=CARTESIAN_POINT('',(-9.,-4.43126136457566,10.));
#20292=CARTESIAN_POINT('Origin',(-9.,-4.5,9.85));
#20293=CARTESIAN_POINT('',(-10.1,-4.43126136457566,10.));
#20294=CARTESIAN_POINT('Origin',(-10.1,-4.5,6.15));
#20295=CARTESIAN_POINT('',(-10.,-4.5,6.315));
#20296=CARTESIAN_POINT('Origin',(-10.,-4.5,6.15));
#20297=CARTESIAN_POINT('',(-9.,-4.5,6.315));
#20298=CARTESIAN_POINT('',(-10.1,-4.5,6.315));
#20299=CARTESIAN_POINT('Origin',(-9.,-4.5,6.15));
#20300=CARTESIAN_POINT('Origin',(-9.5,-4.5,10.));
#20301=CARTESIAN_POINT('',(-10.,-9.,10.));
#20302=CARTESIAN_POINT('',(-10.,0.,10.));
#20303=CARTESIAN_POINT('',(-9.,-9.,10.));
#20304=CARTESIAN_POINT('',(-10.,-9.,10.));
#20305=CARTESIAN_POINT('',(-9.,-9.,10.));
#20306=CARTESIAN_POINT('',(-9.9,-8.2,10.));
#20307=CARTESIAN_POINT('Origin',(-9.5,-8.2,10.));
#20308=CARTESIAN_POINT('Origin',(-9.,-9.,1.));
#20309=CARTESIAN_POINT('',(-9.,-9.,1.));
#20310=CARTESIAN_POINT('',(-9.,-9.,1.));
#20311=CARTESIAN_POINT('',(-9.,0.,1.));
#20312=CARTESIAN_POINT('',(-9.,-9.,1.));
#20313=CARTESIAN_POINT('',(-9.,0.,10.));
#20314=CARTESIAN_POINT('',(-9.,0.,1.));
#20315=CARTESIAN_POINT('',(-9.,-9.,10.));
#20316=CARTESIAN_POINT('',(-9.,-2.,8.605));
#20317=CARTESIAN_POINT('Origin',(-9.,-2.,8.));
#20318=CARTESIAN_POINT('',(-9.,-7.,8.605));
#20319=CARTESIAN_POINT('Origin',(-9.,-7.,8.));
#20320=CARTESIAN_POINT('',(-9.,-4.5,9.6));
#20321=CARTESIAN_POINT('Origin',(-9.,-4.5,8.));
#20322=CARTESIAN_POINT('Origin',(-9.5,-0.8,1.8));
#20323=CARTESIAN_POINT('',(-9.9,-0.8,1.8));
#20324=CARTESIAN_POINT('Origin',(-9.5,-0.8,1.8));
#20325=CARTESIAN_POINT('',(-9.9,-0.8,10.));
#20326=CARTESIAN_POINT('',(-9.9,-0.8,1.8));
#20327=CARTESIAN_POINT('Origin',(-9.5,-0.8,10.));
#20328=CARTESIAN_POINT('Origin',(-9.5,-0.8,1.8));
#20329=CARTESIAN_POINT('',(-9.725,-0.8,1.8));
#20330=CARTESIAN_POINT('Origin',(-9.5,-0.8,1.8));
#20331=CARTESIAN_POINT('Origin',(-9.5,-0.8,0.9));
#20332=CARTESIAN_POINT('',(-9.725,-0.8,1.));
#20333=CARTESIAN_POINT('Origin',(-9.5,-0.8,1.));
#20334=CARTESIAN_POINT('',(-9.725,-0.8,0.9));
#20335=CARTESIAN_POINT('Origin',(-9.5,-8.2,1.8));
#20336=CARTESIAN_POINT('',(-9.9,-8.2,1.8));
#20337=CARTESIAN_POINT('Origin',(-9.5,-8.2,1.8));
#20338=CARTESIAN_POINT('',(-9.9,-8.2,1.8));
#20339=CARTESIAN_POINT('Origin',(-9.5,-8.2,1.8));
#20340=CARTESIAN_POINT('',(-9.725,-8.2,1.8));
#20341=CARTESIAN_POINT('Origin',(-9.5,-8.2,1.8));
#20342=CARTESIAN_POINT('Origin',(-9.5,-8.2,0.9));
#20343=CARTESIAN_POINT('',(-9.725,-8.2,1.));
#20344=CARTESIAN_POINT('Origin',(-9.5,-8.2,1.));
#20345=CARTESIAN_POINT('',(-9.725,-8.2,0.9));
#20346=CARTESIAN_POINT('Origin',(-10.1,-4.5,8.));
#20347=CARTESIAN_POINT('',(-10.,-4.5,9.6));
#20348=CARTESIAN_POINT('Origin',(-10.,-4.5,8.));
#20349=CARTESIAN_POINT('',(-10.1,-4.5,9.6));
#20350=CARTESIAN_POINT('Origin',(-10.1,-7.,8.));
#20351=CARTESIAN_POINT('',(-10.,-7.,8.605));
#20352=CARTESIAN_POINT('Origin',(-10.,-7.,8.));
#20353=CARTESIAN_POINT('',(-10.1,-7.,8.605));
#20354=CARTESIAN_POINT('Origin',(-10.1,-2.,8.));
#20355=CARTESIAN_POINT('',(-10.,-2.,8.605));
#20356=CARTESIAN_POINT('Origin',(-10.,-2.,8.));
#20357=CARTESIAN_POINT('',(-10.1,-2.,8.605));
#20358=CARTESIAN_POINT('Origin',(-9.,0.,1.));
#20359=CARTESIAN_POINT('',(-10.,0.,1.));
#20360=CARTESIAN_POINT('',(-9.,0.,1.));
#20361=CARTESIAN_POINT('',(-10.,0.,10.));
#20362=CARTESIAN_POINT('',(-10.,0.,1.));
#20363=CARTESIAN_POINT('',(-9.,0.,10.));
#20364=CARTESIAN_POINT('Origin',(-10.,-9.,1.));
#20365=CARTESIAN_POINT('',(-10.,-9.,1.));
#20366=CARTESIAN_POINT('',(-10.,-9.,1.));
#20367=CARTESIAN_POINT('',(-10.,-9.,1.));
#20368=CARTESIAN_POINT('Origin',(-10.,0.,1.));
#20369=CARTESIAN_POINT('',(-10.,0.,10.));
#20370=CARTESIAN_POINT('',(-10.,0.,1.));
#20371=CARTESIAN_POINT('Origin',(-9.5,-4.5,10.));
#20372=CARTESIAN_POINT('Origin',(-9.5,-4.5,1.));
#23510=UNCERTAINTY_MEASURE_WITH_UNIT(LENGTH_MEASURE(0.001),#23729,
'DISTANCE_ACCURACY_VALUE',
'Maximum model space distance between geometric entities at asserted c
onnectivities');
#23611=UNCERTAINTY_MEASURE_WITH_UNIT(LENGTH_MEASURE(0.001),#23729,
'DISTANCE_ACCURACY_VALUE',
'Maximum model space distance between geometric entities at asserted c
onnectivities');
#23627=(
GEOMETRIC_REPRESENTATION_CONTEXT(3)
GLOBAL_UNCERTAINTY_ASSIGNED_CONTEXT((#23510))
GLOBAL_UNIT_ASSIGNED_CONTEXT((#23729,#23731,#23732))
REPRESENTATION_CONTEXT('','3D')
);
#23728=(
GEOMETRIC_REPRESENTATION_CONTEXT(3)
GLOBAL_UNCERTAINTY_ASSIGNED_CONTEXT((#23611))
GLOBAL_UNIT_ASSIGNED_CONTEXT((#23729,#23731,#23732))
REPRESENTATION_CONTEXT('','3D')
);
#23729=(
LENGTH_UNIT()
NAMED_UNIT(*)
SI_UNIT(.CENTI.,.METRE.)
);
#23731=(
NAMED_UNIT(*)
PLANE_ANGLE_UNIT()
SI_UNIT($,.RADIAN.)
);
#23732=(
NAMED_UNIT(*)
SI_UNIT($,.STERADIAN.)
SOLID_ANGLE_UNIT()
);
#23748=SHAPE_DEFINITION_REPRESENTATION(#23864,#24127);
#23864=PRODUCT_DEFINITION_SHAPE('',$,#24244);
#24127=SHAPE_REPRESENTATION('',(#13913),#23627);
#24228=PRODUCT_DEFINITION_CONTEXT('part definition',#24578,'design');
#24244=PRODUCT_DEFINITION('Screw and guide support',
'Screw and guide support',#24360,#24228);
#24360=PRODUCT_DEFINITION_FORMATION('',$,#24595);
#24578=APPLICATION_CONTEXT(
'Core Data for Automotive Mechanical Design Process');
#24579=PRODUCT_CONTEXT('part definition',#24578,'mechanical');
#24595=PRODUCT('Screw and guide support','Screw and guide support',
'Screw and guide support',(#24579));
#24766=COLOUR_RGB('Black',0.12,0.14,0.17);
#24767=FILL_AREA_STYLE_COLOUR('',#24766);
#24768=FILL_AREA_STYLE('',(#24767));
#24769=SURFACE_STYLE_FILL_AREA(#24768);
#24770=SURFACE_SIDE_STYLE('',(#24769));
#24771=SURFACE_STYLE_USAGE(.BOTH.,#24770);
#24772=PRESENTATION_STYLE_ASSIGNMENT((#24771));
ENDSEC;
END-ISO-10303-21;
